ISO-10303-21;
HEADER;
/* Generated by software containing ST-Developer
 * from STEP Tools, Inc. (www.steptools.com) 
 */

FILE_DESCRIPTION(
/* description */ ('Belt-driven linear axis on 2020 extrusion'),
/* implementation_level */ '2;1');

FILE_NAME(
/* name */ 'Cap Screw - M5x20.step',
/* time_stamp */ '2026-10-28T03:26:09-07:00',
/* author */ (''),
/* organization */ (''),
/* preprocessor_version */ 'ST-DEVELOPER v20.2',
/* originating_system */ 'Autodesk Translation Framework v15.17.0.0',
/* authorisation */ '');

FILE_SCHEMA (('AUTOMOTIVE_DESIGN { 1 0 10303 214 3 1 1 }'));
ENDSEC;

DATA;
#10=MECHANICAL_DESIGN_GEOMETRIC_PRESENTATION_REPRESENTATION('',(#663),#20096);
#12=ORIENTED_CLOSED_SHELL('',*,#10978,.F.);
#16=BREP_WITH_VOIDS('Body1',#10977,(#12));
#505=CONICAL_SURFACE('',#12615,0.4,0.785398163397448);
#506=CONICAL_SURFACE('',#12619,0.41,0.785398163397448);
#507=CONICAL_SURFACE('',#12623,0.26,0.463647609000806);
#508=CONICAL_SURFACE('',#12627,0.225,0.785398163397448);
#561=SHAPE_REPRESENTATION_RELATIONSHIP('SRR','None',#20362,#607);
#607=ADVANCED_BREP_SHAPE_REPRESENTATION('',(#16),#20093);
#663=STYLED_ITEM('',(#20657),#16);
#886=FACE_BOUND('',#2617,.T.);
#1217=PLANE('',#12613);
#1218=PLANE('',#12621);
#1219=PLANE('',#12629);
#1220=PLANE('',#12630);
#1221=PLANE('',#12631);
#1222=PLANE('',#12632);
#1223=PLANE('',#12633);
#1224=PLANE('',#12634);
#1225=PLANE('',#12635);
#1226=PLANE('',#12636);
#1227=PLANE('',#12637);
#1822=FACE_OUTER_BOUND('',#2612,.T.);
#1823=FACE_OUTER_BOUND('',#2613,.T.);
#1824=FACE_OUTER_BOUND('',#2614,.T.);
#1825=FACE_OUTER_BOUND('',#2615,.T.);
#1826=FACE_OUTER_BOUND('',#2616,.T.);
#1827=FACE_OUTER_BOUND('',#2618,.T.);
#1828=FACE_OUTER_BOUND('',#2619,.T.);
#1829=FACE_OUTER_BOUND('',#2620,.T.);
#1830=FACE_OUTER_BOUND('',#2621,.T.);
#1831=FACE_OUTER_BOUND('',#2622,.T.);
#1832=FACE_OUTER_BOUND('',#2623,.T.);
#1833=FACE_OUTER_BOUND('',#2624,.T.);
#1834=FACE_OUTER_BOUND('',#2625,.T.);
#1835=FACE_OUTER_BOUND('',#2626,.T.);
#1836=FACE_OUTER_BOUND('',#2627,.T.);
#1837=FACE_OUTER_BOUND('',#2628,.T.);
#1838=FACE_OUTER_BOUND('',#2629,.T.);
#2612=EDGE_LOOP('',(#9889));
#2613=EDGE_LOOP('',(#9890,#9891,#9892,#9893));
#2614=EDGE_LOOP('',(#9894,#9895,#9896,#9897));
#2615=EDGE_LOOP('',(#9898,#9899,#9900,#9901));
#2616=EDGE_LOOP('',(#9902));
#2617=EDGE_LOOP('',(#9903));
#2618=EDGE_LOOP('',(#9904,#9905,#9906,#9907));
#2619=EDGE_LOOP('',(#9908,#9909,#9910,#9911));
#2620=EDGE_LOOP('',(#9912,#9913,#9914,#9915));
#2621=EDGE_LOOP('',(#9916));
#2622=EDGE_LOOP('',(#9917,#9918,#9919,#9920));
#2623=EDGE_LOOP('',(#9921,#9922,#9923,#9924));
#2624=EDGE_LOOP('',(#9925,#9926,#9927,#9928));
#2625=EDGE_LOOP('',(#9929,#9930,#9931,#9932));
#2626=EDGE_LOOP('',(#9933,#9934,#9935,#9936));
#2627=EDGE_LOOP('',(#9937,#9938,#9939,#9940));
#2628=EDGE_LOOP('',(#9941,#9942,#9943,#9944,#9945,#9946));
#2629=EDGE_LOOP('',(#9947,#9948,#9949,#9950,#9951,#9952));
#3451=LINE('',#19693,#4308);
#3452=LINE('',#19697,#4309);
#3453=LINE('',#19701,#4310);
#3454=LINE('',#19708,#4311);
#3455=LINE('',#19712,#4312);
#3456=LINE('',#19716,#4313);
#3457=LINE('',#19721,#4314);
#3458=LINE('',#19723,#4315);
#3459=LINE('',#19725,#4316);
#3460=LINE('',#19726,#4317);
#3461=LINE('',#19729,#4318);
#3462=LINE('',#19731,#4319);
#3463=LINE('',#19732,#4320);
#3464=LINE('',#19735,#4321);
#3465=LINE('',#19737,#4322);
#3466=LINE('',#19738,#4323);
#3467=LINE('',#19741,#4324);
#3468=LINE('',#19743,#4325);
#3469=LINE('',#19744,#4326);
#3470=LINE('',#19747,#4327);
#3471=LINE('',#19749,#4328);
#3472=LINE('',#19750,#4329);
#3473=LINE('',#19752,#4330);
#3474=LINE('',#19753,#4331);
#4308=VECTOR('',#15825,0.4);
#4309=VECTOR('',#15830,0.425);
#4310=VECTOR('',#15835,0.41);
#4311=VECTOR('',#15844,0.26);
#4312=VECTOR('',#15849,0.25);
#4313=VECTOR('',#15854,0.225);
#4314=VECTOR('',#15859,1.);
#4315=VECTOR('',#15860,1.);
#4316=VECTOR('',#15861,1.);
#4317=VECTOR('',#15862,1.);
#4318=VECTOR('',#15865,1.);
#4319=VECTOR('',#15866,1.);
#4320=VECTOR('',#15867,1.);
#4321=VECTOR('',#15870,1.);
#4322=VECTOR('',#15871,1.);
#4323=VECTOR('',#15872,1.);
#4324=VECTOR('',#15875,1.);
#4325=VECTOR('',#15876,1.);
#4326=VECTOR('',#15877,1.);
#4327=VECTOR('',#15880,1.);
#4328=VECTOR('',#15881,1.);
#4329=VECTOR('',#15882,1.);
#4330=VECTOR('',#15885,1.);
#4331=VECTOR('',#15886,1.);
#4869=CIRCLE('',#12614,0.375);
#4870=CIRCLE('',#12616,0.425);
#4871=CIRCLE('',#12618,0.425);
#4872=CIRCLE('',#12620,0.395);
#4873=CIRCLE('',#12622,0.27);
#4874=CIRCLE('',#12624,0.24505);
#4875=CIRCLE('',#12626,0.24505);
#4876=CIRCLE('',#12628,0.2);
#5782=VERTEX_POINT('',#19688);
#5783=VERTEX_POINT('',#19691);
#5784=VERTEX_POINT('',#19695);
#5785=VERTEX_POINT('',#19699);
#5786=VERTEX_POINT('',#19703);
#5787=VERTEX_POINT('',#19706);
#5788=VERTEX_POINT('',#19710);
#5789=VERTEX_POINT('',#19714);
#5790=VERTEX_POINT('',#19719);
#5791=VERTEX_POINT('',#19720);
#5792=VERTEX_POINT('',#19722);
#5793=VERTEX_POINT('',#19724);
#5794=VERTEX_POINT('',#19728);
#5795=VERTEX_POINT('',#19730);
#5796=VERTEX_POINT('',#19734);
#5797=VERTEX_POINT('',#19736);
#5798=VERTEX_POINT('',#19740);
#5799=VERTEX_POINT('',#19742);
#5800=VERTEX_POINT('',#19746);
#5801=VERTEX_POINT('',#19748);
#7159=EDGE_CURVE('',#5782,#5782,#4869,.T.);
#7160=EDGE_CURVE('',#5783,#5783,#4870,.T.);
#7161=EDGE_CURVE('',#5783,#5782,#3451,.T.);
#7162=EDGE_CURVE('',#5784,#5784,#4871,.T.);
#7163=EDGE_CURVE('',#5784,#5783,#3452,.T.);
#7164=EDGE_CURVE('',#5785,#5785,#4872,.T.);
#7165=EDGE_CURVE('',#5785,#5784,#3453,.T.);
#7166=EDGE_CURVE('',#5786,#5786,#4873,.T.);
#7167=EDGE_CURVE('',#5787,#5787,#4874,.F.);
#7168=EDGE_CURVE('',#5787,#5786,#3454,.T.);
#7169=EDGE_CURVE('',#5788,#5788,#4875,.F.);
#7170=EDGE_CURVE('',#5788,#5787,#3455,.T.);
#7171=EDGE_CURVE('',#5789,#5789,#4876,.T.);
#7172=EDGE_CURVE('',#5789,#5788,#3456,.T.);
#7173=EDGE_CURVE('',#5790,#5791,#3457,.T.);
#7174=EDGE_CURVE('',#5791,#5792,#3458,.T.);
#7175=EDGE_CURVE('',#5792,#5793,#3459,.T.);
#7176=EDGE_CURVE('',#5790,#5793,#3460,.T.);
#7177=EDGE_CURVE('',#5791,#5794,#3461,.T.);
#7178=EDGE_CURVE('',#5794,#5795,#3462,.T.);
#7179=EDGE_CURVE('',#5795,#5792,#3463,.T.);
#7180=EDGE_CURVE('',#5794,#5796,#3464,.T.);
#7181=EDGE_CURVE('',#5796,#5797,#3465,.T.);
#7182=EDGE_CURVE('',#5797,#5795,#3466,.T.);
#7183=EDGE_CURVE('',#5796,#5798,#3467,.T.);
#7184=EDGE_CURVE('',#5798,#5799,#3468,.T.);
#7185=EDGE_CURVE('',#5799,#5797,#3469,.T.);
#7186=EDGE_CURVE('',#5798,#5800,#3470,.T.);
#7187=EDGE_CURVE('',#5800,#5801,#3471,.T.);
#7188=EDGE_CURVE('',#5801,#5799,#3472,.T.);
#7189=EDGE_CURVE('',#5800,#5790,#3473,.T.);
#7190=EDGE_CURVE('',#5793,#5801,#3474,.T.);
#9889=ORIENTED_EDGE('',*,*,#7159,.F.);
#9890=ORIENTED_EDGE('',*,*,#7160,.F.);
#9891=ORIENTED_EDGE('',*,*,#7161,.T.);
#9892=ORIENTED_EDGE('',*,*,#7159,.T.);
#9893=ORIENTED_EDGE('',*,*,#7161,.F.);
#9894=ORIENTED_EDGE('',*,*,#7162,.F.);
#9895=ORIENTED_EDGE('',*,*,#7163,.T.);
#9896=ORIENTED_EDGE('',*,*,#7160,.T.);
#9897=ORIENTED_EDGE('',*,*,#7163,.F.);
#9898=ORIENTED_EDGE('',*,*,#7164,.F.);
#9899=ORIENTED_EDGE('',*,*,#7165,.T.);
#9900=ORIENTED_EDGE('',*,*,#7162,.T.);
#9901=ORIENTED_EDGE('',*,*,#7165,.F.);
#9902=ORIENTED_EDGE('',*,*,#7164,.T.);
#9903=ORIENTED_EDGE('',*,*,#7166,.F.);
#9904=ORIENTED_EDGE('',*,*,#7167,.F.);
#9905=ORIENTED_EDGE('',*,*,#7168,.T.);
#9906=ORIENTED_EDGE('',*,*,#7166,.T.);
#9907=ORIENTED_EDGE('',*,*,#7168,.F.);
#9908=ORIENTED_EDGE('',*,*,#7169,.F.);
#9909=ORIENTED_EDGE('',*,*,#7170,.T.);
#9910=ORIENTED_EDGE('',*,*,#7167,.T.);
#9911=ORIENTED_EDGE('',*,*,#7170,.F.);
#9912=ORIENTED_EDGE('',*,*,#7171,.F.);
#9913=ORIENTED_EDGE('',*,*,#7172,.T.);
#9914=ORIENTED_EDGE('',*,*,#7169,.T.);
#9915=ORIENTED_EDGE('',*,*,#7172,.F.);
#9916=ORIENTED_EDGE('',*,*,#7171,.T.);
#9917=ORIENTED_EDGE('',*,*,#7173,.T.);
#9918=ORIENTED_EDGE('',*,*,#7174,.T.);
#9919=ORIENTED_EDGE('',*,*,#7175,.T.);
#9920=ORIENTED_EDGE('',*,*,#7176,.F.);
#9921=ORIENTED_EDGE('',*,*,#7177,.T.);
#9922=ORIENTED_EDGE('',*,*,#7178,.T.);
#9923=ORIENTED_EDGE('',*,*,#7179,.T.);
#9924=ORIENTED_EDGE('',*,*,#7174,.F.);
#9925=ORIENTED_EDGE('',*,*,#7180,.T.);
#9926=ORIENTED_EDGE('',*,*,#7181,.T.);
#9927=ORIENTED_EDGE('',*,*,#7182,.T.);
#9928=ORIENTED_EDGE('',*,*,#7178,.F.);
#9929=ORIENTED_EDGE('',*,*,#7183,.T.);
#9930=ORIENTED_EDGE('',*,*,#7184,.T.);
#9931=ORIENTED_EDGE('',*,*,#7185,.T.);
#9932=ORIENTED_EDGE('',*,*,#7181,.F.);
#9933=ORIENTED_EDGE('',*,*,#7186,.T.);
#9934=ORIENTED_EDGE('',*,*,#7187,.T.);
#9935=ORIENTED_EDGE('',*,*,#7188,.T.);
#9936=ORIENTED_EDGE('',*,*,#7184,.F.);
#9937=ORIENTED_EDGE('',*,*,#7189,.T.);
#9938=ORIENTED_EDGE('',*,*,#7176,.T.);
#9939=ORIENTED_EDGE('',*,*,#7190,.T.);
#9940=ORIENTED_EDGE('',*,*,#7187,.F.);
#9941=ORIENTED_EDGE('',*,*,#7189,.F.);
#9942=ORIENTED_EDGE('',*,*,#7186,.F.);
#9943=ORIENTED_EDGE('',*,*,#7183,.F.);
#9944=ORIENTED_EDGE('',*,*,#7180,.F.);
#9945=ORIENTED_EDGE('',*,*,#7177,.F.);
#9946=ORIENTED_EDGE('',*,*,#7173,.F.);
#9947=ORIENTED_EDGE('',*,*,#7190,.F.);
#9948=ORIENTED_EDGE('',*,*,#7175,.F.);
#9949=ORIENTED_EDGE('',*,*,#7179,.F.);
#9950=ORIENTED_EDGE('',*,*,#7182,.F.);
#9951=ORIENTED_EDGE('',*,*,#7185,.F.);
#9952=ORIENTED_EDGE('',*,*,#7188,.F.);
#10295=CYLINDRICAL_SURFACE('',#12617,0.425);
#10296=CYLINDRICAL_SURFACE('',#12625,0.24505);
#10873=ADVANCED_FACE('',(#1822),#1217,.T.);
#10874=ADVANCED_FACE('',(#1823),#505,.T.);
#10875=ADVANCED_FACE('',(#1824),#10295,.T.);
#10876=ADVANCED_FACE('',(#1825),#506,.T.);
#10877=ADVANCED_FACE('',(#1826,#886),#1218,.T.);
#10878=ADVANCED_FACE('',(#1827),#507,.T.);
#10879=ADVANCED_FACE('',(#1828),#10296,.T.);
#10880=ADVANCED_FACE('',(#1829),#508,.T.);
#10881=ADVANCED_FACE('',(#1830),#1219,.T.);
#10882=ADVANCED_FACE('',(#1831),#1220,.F.);
#10883=ADVANCED_FACE('',(#1832),#1221,.F.);
#10884=ADVANCED_FACE('',(#1833),#1222,.F.);
#10885=ADVANCED_FACE('',(#1834),#1223,.F.);
#10886=ADVANCED_FACE('',(#1835),#1224,.F.);
#10887=ADVANCED_FACE('',(#1836),#1225,.F.);
#10888=ADVANCED_FACE('',(#1837),#1226,.F.);
#10889=ADVANCED_FACE('',(#1838),#1227,.F.);
#10977=CLOSED_SHELL('',(#10873,#10874,#10875,#10876,#10877,#10878,#10879,
#10880,#10881));
#10978=CLOSED_SHELL('',(#10882,#10883,#10884,#10885,#10886,#10887,#10888,
#10889));
#12612=AXIS2_PLACEMENT_3D('',#19686,#15815,#15816);
#12613=AXIS2_PLACEMENT_3D('',#19687,#15817,#15818);
#12614=AXIS2_PLACEMENT_3D('',#19689,#15819,#15820);
#12615=AXIS2_PLACEMENT_3D('',#19690,#15821,#15822);
#12616=AXIS2_PLACEMENT_3D('',#19692,#15823,#15824);
#12617=AXIS2_PLACEMENT_3D('',#19694,#15826,#15827);
#12618=AXIS2_PLACEMENT_3D('',#19696,#15828,#15829);
#12619=AXIS2_PLACEMENT_3D('',#19698,#15831,#15832);
#12620=AXIS2_PLACEMENT_3D('',#19700,#15833,#15834);
#12621=AXIS2_PLACEMENT_3D('',#19702,#15836,#15837);
#12622=AXIS2_PLACEMENT_3D('',#19704,#15838,#15839);
#12623=AXIS2_PLACEMENT_3D('',#19705,#15840,#15841);
#12624=AXIS2_PLACEMENT_3D('',#19707,#15842,#15843);
#12625=AXIS2_PLACEMENT_3D('',#19709,#15845,#15846);
#12626=AXIS2_PLACEMENT_3D('',#19711,#15847,#15848);
#12627=AXIS2_PLACEMENT_3D('',#19713,#15850,#15851);
#12628=AXIS2_PLACEMENT_3D('',#19715,#15852,#15853);
#12629=AXIS2_PLACEMENT_3D('',#19717,#15855,#15856);
#12630=AXIS2_PLACEMENT_3D('',#19718,#15857,#15858);
#12631=AXIS2_PLACEMENT_3D('',#19727,#15863,#15864);
#12632=AXIS2_PLACEMENT_3D('',#19733,#15868,#15869);
#12633=AXIS2_PLACEMENT_3D('',#19739,#15873,#15874);
#12634=AXIS2_PLACEMENT_3D('',#19745,#15878,#15879);
#12635=AXIS2_PLACEMENT_3D('',#19751,#15883,#15884);
#12636=AXIS2_PLACEMENT_3D('',#19754,#15887,#15888);
#12637=AXIS2_PLACEMENT_3D('',#19755,#15889,#15890);
#15815=DIRECTION('axis',(0.,0.,1.));
#15816=DIRECTION('refdir',(1.,0.,0.));
#15817=DIRECTION('center_axis',(0.,1.,0.));
#15818=DIRECTION('ref_axis',(0.,0.,1.));
#15819=DIRECTION('center_axis',(0.,-1.,0.));
#15820=DIRECTION('ref_axis',(1.,0.,0.));
#15821=DIRECTION('center_axis',(0.,-1.,0.));
#15822=DIRECTION('ref_axis',(1.,0.,0.));
#15823=DIRECTION('center_axis',(0.,-1.,0.));
#15824=DIRECTION('ref_axis',(1.,0.,0.));
#15825=DIRECTION('',(0.707106781186548,0.707106781186547,8.65956056235493E-17));
#15826=DIRECTION('center_axis',(0.,-1.,0.));
#15827=DIRECTION('ref_axis',(1.,0.,0.));
#15828=DIRECTION('center_axis',(0.,-1.,0.));
#15829=DIRECTION('ref_axis',(1.,0.,0.));
#15830=DIRECTION('',(0.,1.,0.));
#15831=DIRECTION('center_axis',(0.,1.,0.));
#15832=DIRECTION('ref_axis',(1.,0.,0.));
#15833=DIRECTION('center_axis',(0.,-1.,0.));
#15834=DIRECTION('ref_axis',(1.,0.,0.));
#15835=DIRECTION('',(-0.707106781186547,0.707106781186548,-8.65956056235493E-17));
#15836=DIRECTION('center_axis',(0.,-1.,0.));
#15837=DIRECTION('ref_axis',(0.,0.,-1.));
#15838=DIRECTION('center_axis',(0.,-1.,0.));
#15839=DIRECTION('ref_axis',(1.,0.,0.));
#15840=DIRECTION('center_axis',(0.,1.,0.));
#15841=DIRECTION('ref_axis',(1.,0.,0.));
#15842=DIRECTION('center_axis',(0.,1.,0.));
#15843=DIRECTION('ref_axis',(1.,0.,0.));
#15844=DIRECTION('',(-0.447213595499958,0.894427190999916,-5.47678698264203E-17));
#15845=DIRECTION('center_axis',(0.,-1.,0.));
#15846=DIRECTION('ref_axis',(1.,0.,0.));
#15847=DIRECTION('center_axis',(0.,1.,0.));
#15848=DIRECTION('ref_axis',(1.,0.,0.));
#15849=DIRECTION('',(0.,1.,0.));
#15850=DIRECTION('center_axis',(0.,1.,0.));
#15851=DIRECTION('ref_axis',(1.,0.,0.));
#15852=DIRECTION('center_axis',(0.,-1.,0.));
#15853=DIRECTION('ref_axis',(1.,0.,0.));
#15854=DIRECTION('',(-0.707106781186547,0.707106781186548,-8.65956056235493E-17));
#15855=DIRECTION('center_axis',(0.,-1.,0.));
#15856=DIRECTION('ref_axis',(0.,0.,-1.));
#15857=DIRECTION('center_axis',(0.866025403784439,0.,-0.5));
#15858=DIRECTION('ref_axis',(0.5,0.,0.866025403784439));
#15859=DIRECTION('',(-0.5,0.,-0.866025403784439));
#15860=DIRECTION('',(0.,-1.,0.));
#15861=DIRECTION('',(0.5,0.,0.866025403784439));
#15862=DIRECTION('',(0.,-1.,0.));
#15863=DIRECTION('center_axis',(1.20185167898973E-16,0.,-1.));
#15864=DIRECTION('ref_axis',(1.,0.,1.20185167898973E-16));
#15865=DIRECTION('',(-1.,0.,-1.20185167898973E-16));
#15866=DIRECTION('',(0.,-1.,0.));
#15867=DIRECTION('',(1.,0.,1.20185167898973E-16));
#15868=DIRECTION('center_axis',(-0.866025403784439,0.,-0.5));
#15869=DIRECTION('ref_axis',(0.5,0.,-0.866025403784439));
#15870=DIRECTION('',(-0.5,0.,0.866025403784439));
#15871=DIRECTION('',(0.,-1.,0.));
#15872=DIRECTION('',(0.5,0.,-0.866025403784439));
#15873=DIRECTION('center_axis',(-0.866025403784439,0.,0.5));
#15874=DIRECTION('ref_axis',(-0.5,0.,-0.866025403784439));
#15875=DIRECTION('',(0.5,0.,0.866025403784439));
#15876=DIRECTION('',(0.,-1.,0.));
#15877=DIRECTION('',(-0.5,0.,-0.866025403784439));
#15878=DIRECTION('center_axis',(-2.40370335797945E-16,0.,1.));
#15879=DIRECTION('ref_axis',(-1.,0.,-2.40370335797945E-16));
#15880=DIRECTION('',(1.,0.,2.40370335797945E-16));
#15881=DIRECTION('',(0.,-1.,0.));
#15882=DIRECTION('',(-1.,0.,-2.40370335797945E-16));
#15883=DIRECTION('center_axis',(0.866025403784439,0.,0.5));
#15884=DIRECTION('ref_axis',(-0.5,0.,0.866025403784439));
#15885=DIRECTION('',(0.5,0.,-0.866025403784439));
#15886=DIRECTION('',(-0.5,0.,0.866025403784439));
#15887=DIRECTION('center_axis',(0.,1.,0.));
#15888=DIRECTION('ref_axis',(1.,0.,0.));
#15889=DIRECTION('center_axis',(0.,-1.,0.));
#15890=DIRECTION('ref_axis',(0.,0.,-1.));
#19686=CARTESIAN_POINT('',(0.,0.,0.));
#19687=CARTESIAN_POINT('Origin',(0.375,0.5,0.));
#19688=CARTESIAN_POINT('',(-0.375,0.5,-4.59242549680257E-17));
#19689=CARTESIAN_POINT('Origin',(0.,0.5,0.));
#19690=CARTESIAN_POINT('Origin',(0.,0.475,0.));
#19691=CARTESIAN_POINT('',(-0.425,0.45,-5.20474889637625E-17));
#19692=CARTESIAN_POINT('Origin',(0.,0.45,0.));
#19693=CARTESIAN_POINT('',(-0.4,0.475,-4.89858719658941E-17));
#19694=CARTESIAN_POINT('Origin',(0.,0.24,0.));
#19695=CARTESIAN_POINT('',(-0.425,0.0299999999999998,-5.20474889637625E-17));
#19696=CARTESIAN_POINT('Origin',(0.,0.0299999999999998,0.));
#19697=CARTESIAN_POINT('',(-0.425,0.24,-5.20474889637625E-17));
#19698=CARTESIAN_POINT('Origin',(0.,0.0150000000000001,0.));
#19699=CARTESIAN_POINT('',(-0.395,4.85722573273506E-17,-4.83735485663204E-17));
#19700=CARTESIAN_POINT('Origin',(0.,0.,0.));
#19701=CARTESIAN_POINT('',(-0.41,0.0150000000000001,-5.02105187650415E-17));
#19702=CARTESIAN_POINT('Origin',(0.27,0.,0.));
#19703=CARTESIAN_POINT('',(-0.27,0.,-3.30654635769785E-17));
#19704=CARTESIAN_POINT('Origin',(0.,0.,0.));
#19705=CARTESIAN_POINT('Origin',(0.,-0.02,0.));
#19706=CARTESIAN_POINT('',(-0.24505,-0.0498999999999999,3.00099698131059E-17));
#19707=CARTESIAN_POINT('Origin',(0.,-0.0498999999999999,0.));
#19708=CARTESIAN_POINT('',(-0.26,-0.02,-3.18408167778312E-17));
#19709=CARTESIAN_POINT('Origin',(0.,-0.995,0.));
#19710=CARTESIAN_POINT('',(-0.24505,-1.95495,3.00099698131059E-17));
#19711=CARTESIAN_POINT('Origin',(0.,-1.95495,0.));
#19712=CARTESIAN_POINT('',(-0.24505,-0.995,-3.00099698131059E-17));
#19713=CARTESIAN_POINT('Origin',(0.,-1.975,0.));
#19714=CARTESIAN_POINT('',(-0.2,-2.,-2.44929359829471E-17));
#19715=CARTESIAN_POINT('Origin',(0.,-2.,0.));
#19716=CARTESIAN_POINT('',(-0.225,-1.975,-2.75545529808154E-17));
#19717=CARTESIAN_POINT('Origin',(0.,-2.,0.));
#19718=CARTESIAN_POINT('Origin',(0.115470053837925,-0.5,-0.2));
#19719=CARTESIAN_POINT('',(0.23094010767585,-0.5,0.));
#19720=CARTESIAN_POINT('',(0.115470053837925,-0.5,-0.2));
#19721=CARTESIAN_POINT('',(0.23094010767585,-0.5,0.));
#19722=CARTESIAN_POINT('',(0.115470053837925,-0.8,-0.2));
#19723=CARTESIAN_POINT('',(0.115470053837925,-0.5,-0.2));
#19724=CARTESIAN_POINT('',(0.23094010767585,-0.8,0.));
#19725=CARTESIAN_POINT('',(0.23094010767585,-0.8,0.));
#19726=CARTESIAN_POINT('',(0.23094010767585,-0.5,0.));
#19727=CARTESIAN_POINT('Origin',(-0.115470053837925,-0.5,-0.2));
#19728=CARTESIAN_POINT('',(-0.115470053837925,-0.5,-0.2));
#19729=CARTESIAN_POINT('',(0.115470053837925,-0.5,-0.2));
#19730=CARTESIAN_POINT('',(-0.115470053837925,-0.8,-0.2));
#19731=CARTESIAN_POINT('',(-0.115470053837925,-0.5,-0.2));
#19732=CARTESIAN_POINT('',(0.115470053837925,-0.8,-0.2));
#19733=CARTESIAN_POINT('Origin',(-0.23094010767585,-0.5,-2.77555756156289E-17));
#19734=CARTESIAN_POINT('',(-0.23094010767585,-0.5,-2.82820063659975E-17));
#19735=CARTESIAN_POINT('',(-0.115470053837925,-0.5,-0.2));
#19736=CARTESIAN_POINT('',(-0.23094010767585,-0.8,-2.77555756156289E-17));
#19737=CARTESIAN_POINT('',(-0.23094010767585,-0.5,-2.82820063659975E-17));
#19738=CARTESIAN_POINT('',(-0.115470053837925,-0.8,-0.2));
#19739=CARTESIAN_POINT('Origin',(-0.115470053837925,-0.5,0.2));
#19740=CARTESIAN_POINT('',(-0.115470053837925,-0.5,0.2));
#19741=CARTESIAN_POINT('',(-0.23094010767585,-0.5,-2.82820063659975E-17));
#19742=CARTESIAN_POINT('',(-0.115470053837925,-0.8,0.2));
#19743=CARTESIAN_POINT('',(-0.115470053837925,-0.5,0.2));
#19744=CARTESIAN_POINT('',(-0.23094010767585,-0.8,-2.82820063659975E-17));
#19745=CARTESIAN_POINT('Origin',(0.115470053837925,-0.5,0.2));
#19746=CARTESIAN_POINT('',(0.115470053837925,-0.5,0.2));
#19747=CARTESIAN_POINT('',(-0.115470053837925,-0.5,0.2));
#19748=CARTESIAN_POINT('',(0.115470053837925,-0.8,0.2));
#19749=CARTESIAN_POINT('',(0.115470053837925,-0.5,0.2));
#19750=CARTESIAN_POINT('',(-0.115470053837925,-0.8,0.2));
#19751=CARTESIAN_POINT('Origin',(0.23094010767585,-0.5,0.));
#19752=CARTESIAN_POINT('',(0.115470053837925,-0.5,0.2));
#19753=CARTESIAN_POINT('',(0.115470053837925,-0.8,0.2));
#19754=CARTESIAN_POINT('Origin',(0.,-0.5,0.));
#19755=CARTESIAN_POINT('Origin',(0.,-0.8,0.));
#20039=UNCERTAINTY_MEASURE_WITH_UNIT(LENGTH_MEASURE(0.001),#20097,
'DISTANCE_ACCURACY_VALUE',
'Maximum model space distance between geometric entities at asserted c
onnectivities');
#20042=UNCERTAINTY_MEASURE_WITH_UNIT(LENGTH_MEASURE(0.001),#20097,
'DISTANCE_ACCURACY_VALUE',
'Maximum model space distance between geometric entities at asserted c
onnectivities');
#20093=(
GEOMETRIC_REPRESENTATION_CONTEXT(3)
GLOBAL_UNCERTAINTY_ASSIGNED_CONTEXT((#20039))
GLOBAL_UNIT_ASSIGNED_CONTEXT((#20097,#20099,#20100))
REPRESENTATION_CONTEXT('','3D')
);
#20096=(
GEOMETRIC_REPRESENTATION_CONTEXT(3)
GLOBAL_UNCERTAINTY_ASSIGNED_CONTEXT((#20042))
GLOBAL_UNIT_ASSIGNED_CONTEXT((#20097,#20099,#20100))
REPRESENTATION_CONTEXT('','3D')
);
#20097=(
LENGTH_UNIT()
NAMED_UNIT(*)
SI_UNIT(.CENTI.,.METRE.)
);
#20099=(
NAMED_UNIT(*)
PLANE_ANGLE_UNIT()
SI_UNIT($,.RADIAN.)
);
#20100=(
NAMED_UNIT(*)
SI_UNIT($,.STERADIAN.)
SOLID_ANGLE_UNIT()
);
#20151=SHAPE_DEFINITION_REPRESENTATION(#20212,#20362);
#20212=PRODUCT_DEFINITION_SHAPE('',$,#20416);
#20362=SHAPE_REPRESENTATION('',(#12612),#20093);
#20365=PRODUCT_DEFINITION_CONTEXT('part definition',#20526,'design');
#20416=PRODUCT_DEFINITION('Cap Screw - M5x20','Cap Screw - M5x20',#20469,
#20365);
#20469=PRODUCT_DEFINITION_FORMATION('',$,#20578);
#20526=APPLICATION_CONTEXT(
'Core Data for Automotive Mechanical Design Process');
#20527=PRODUCT_CONTEXT('part definition',#20526,'mechanical');
#20578=PRODUCT('Cap Screw - M5x20','Cap Screw - M5x20',
'Cap Screw - M5x20',(#20527));
#20651=COLOUR_RGB('Black',0.12,0.14,0.17);
#20652=FILL_AREA_STYLE_COLOUR('',#20651);
#20653=FILL_AREA_STYLE('',(#20652));
#20654=SURFACE_STYLE_FILL_AREA(#20653);
#20655=SURFACE_SIDE_STYLE('',(#20654));
#20656=SURFACE_STYLE_USAGE(.BOTH.,#20655);
#20657=PRESENTATION_STYLE_ASSIGNMENT((#20656));
ENDSEC;
END-ISO-10303-21;
